ISO-10303-21;
HEADER;
/* Generated by software containing ST-Developer
 * from STEP Tools, Inc. (www.steptools.com) 
 */

FILE_DESCRIPTION(
/* description */ ('STEP AP203'),
/* implementation_level */ '2;1');

FILE_NAME(
/* name */ 'P12_Jaw_Clamping_Screw.step',
/* time_stamp */ '2026-11-15T15:04:01-08:00',
/* author */ (''),
/* organization */ (''),
/* preprocessor_version */ 'ST-DEVELOPER v20.2',
/* originating_system */ 'Autodesk Translation Framework v15.17.0.0',
/* authorisation */ '');

FILE_SCHEMA (('AUTOMOTIVE_DESIGN { 1 0 10303 214 3 1 1 }'));
ENDSEC;

DATA;
#10=MECHANICAL_DESIGN_GEOMETRIC_PRESENTATION_REPRESENTATION('',(#291),#16598);
#189=B_SPLINE_CURVE_WITH_KNOTS('',3,(#14759,#14760,#14761,#14762,#14763,
#14764,#14765,#14766,#14767,#14768,#14769,#14770,#14771,#14772,#14773,#14774,
#14775,#14776),.UNSPECIFIED.,.F.,.F.,(4,2,2,2,2,2,2,2,4),(1.66329163352374,
1.74645277590797,1.82961391829221,1.91278193926035,1.99594996022848,2.07911798119662,
2.16228600216475,2.24544714454899,2.32860828693323),.UNSPECIFIED.);
#190=B_SPLINE_CURVE_WITH_KNOTS('',3,(#14777,#14778,#14779,#14780,#14781,
#14782,#14783,#14784,#14785,#14786,#14787,#14788,#14789,#14790,#14791,#14792,
#14793,#14794,#14795),.UNSPECIFIED.,.F.,.F.,(4,2,2,2,3,2,2,2,4),(0.997974980114241,
1.08113612249848,1.16429726488272,1.24746528585085,1.33063330681899,1.41380132778712,
1.49696934875526,1.5801304911395,1.66329163352374),.UNSPECIFIED.);
#191=B_SPLINE_CURVE_WITH_KNOTS('',3,(#14799,#14800,#14801,#14802,#14803,
#14804,#14805,#14806,#14807,#14808,#14809,#14810,#14811,#14812,#14813,#14814,
#14815,#14816),.UNSPECIFIED.,.F.,.F.,(4,2,2,2,2,2,2,2,4),(-0.997974980114241,
-0.914813837730002,-0.831652695345763,-0.748484674377629,-0.665316653409494,
-0.58214863244136,-0.498980611473225,-0.415819469088986,-0.332658326704747),
 .UNSPECIFIED.);
#192=B_SPLINE_CURVE_WITH_KNOTS('',3,(#14820,#14821,#14822,#14823,#14824,
#14825,#14826,#14827,#14828,#14829,#14830,#14831,#14832,#14833,#14834,#14835,
#14836,#14837,#14838),.UNSPECIFIED.,.F.,.F.,(4,2,2,2,3,2,2,2,4),(-0.332658326704747,
-0.249497184320508,-0.166336041936269,-0.0831680209681343,0.,0.0831680209681345,
0.166336041936269,0.249497184320508,0.332658326704747),.UNSPECIFIED.);
#213=SHAPE_REPRESENTATION_RELATIONSHIP('SRR','None',#16707,#237);
#237=ADVANCED_BREP_SHAPE_REPRESENTATION('',(#261),#16583);
#261=MANIFOLD_SOLID_BREP('Body1',#9796);
#291=STYLED_ITEM('',(#16833),#261);
#350=FACE_BOUND('',#1723,.T.);
#351=FACE_BOUND('',#1727,.T.);
#352=FACE_BOUND('',#1729,.T.);
#353=FACE_BOUND('',#1732,.T.);
#354=FACE_BOUND('',#1734,.T.);
#607=PLANE('',#10396);
#608=PLANE('',#10397);
#609=PLANE('',#10398);
#610=PLANE('',#10399);
#611=PLANE('',#10400);
#612=PLANE('',#10401);
#613=PLANE('',#10402);
#614=PLANE('',#10403);
#1123=FACE_OUTER_BOUND('',#1718,.T.);
#1124=FACE_OUTER_BOUND('',#1719,.T.);
#1125=FACE_OUTER_BOUND('',#1720,.T.);
#1126=FACE_OUTER_BOUND('',#1721,.T.);
#1127=FACE_OUTER_BOUND('',#1722,.T.);
#1128=FACE_OUTER_BOUND('',#1724,.T.);
#1129=FACE_OUTER_BOUND('',#1725,.T.);
#1130=FACE_OUTER_BOUND('',#1726,.T.);
#1131=FACE_OUTER_BOUND('',#1728,.T.);
#1132=FACE_OUTER_BOUND('',#1730,.T.);
#1133=FACE_OUTER_BOUND('',#1731,.T.);
#1134=FACE_OUTER_BOUND('',#1733,.T.);
#1135=FACE_OUTER_BOUND('',#1735,.T.);
#1718=EDGE_LOOP('',(#7617,#7618,#7619,#7620,#7621));
#1719=EDGE_LOOP('',(#7622,#7623,#7624,#7625,#7626));
#1720=EDGE_LOOP('',(#7627,#7628,#7629,#7630));
#1721=EDGE_LOOP('',(#7631,#7632,#7633,#7634));
#1722=EDGE_LOOP('',(#7635,#7636,#7637,#7638,#7639,#7640,#7641,#7642,#7643,
#7644,#7645,#7646,#7647,#7648,#7649,#7650));
#1723=EDGE_LOOP('',(#7651,#7652));
#1724=EDGE_LOOP('',(#7653,#7654));
#1725=EDGE_LOOP('',(#7655,#7656,#7657));
#1726=EDGE_LOOP('',(#7658));
#1727=EDGE_LOOP('',(#7659));
#1728=EDGE_LOOP('',(#7660));
#1729=EDGE_LOOP('',(#7661));
#1730=EDGE_LOOP('',(#7662));
#1731=EDGE_LOOP('',(#7663,#7664,#7665,#7666));
#1732=EDGE_LOOP('',(#7667));
#1733=EDGE_LOOP('',(#7668,#7669,#7670,#7671));
#1734=EDGE_LOOP('',(#7672));
#1735=EDGE_LOOP('',(#7673,#7674,#7675,#7676));
#2566=LINE('',#14757,#3614);
#2567=LINE('',#14818,#3615);
#2568=LINE('',#14843,#3616);
#2569=LINE('',#14849,#3617);
#2570=LINE('',#14856,#3618);
#2571=LINE('',#14860,#3619);
#2572=LINE('',#14863,#3620);
#2573=LINE('',#14865,#3621);
#2574=LINE('',#14870,#3622);
#2575=LINE('',#14873,#3623);
#2576=LINE('',#14875,#3624);
#2577=LINE('',#14877,#3625);
#2578=LINE('',#14882,#3626);
#2579=LINE('',#14884,#3627);
#3614=VECTOR('',#11968,2.2);
#3615=VECTOR('',#11971,2.2);
#3616=VECTOR('',#11978,6.);
#3617=VECTOR('',#11985,8.75);
#3618=VECTOR('',#11992,1000.);
#3619=VECTOR('',#11995,1000.);
#3620=VECTOR('',#11998,10.);
#3621=VECTOR('',#11999,10.);
#3622=VECTOR('',#12004,1000.);
#3623=VECTOR('',#12007,1000.);
#3624=VECTOR('',#12010,1000.);
#3625=VECTOR('',#12013,1000.);
#3626=VECTOR('',#12022,1000.);
#3627=VECTOR('',#12025,1000.);
#4303=CIRCLE('',#10380,2.2);
#4304=CIRCLE('',#10382,2.2);
#4305=CIRCLE('',#10384,6.);
#4306=CIRCLE('',#10385,6.);
#4307=CIRCLE('',#10387,8.75);
#4308=CIRCLE('',#10388,8.75);
#4309=CIRCLE('',#10390,10.);
#4310=CIRCLE('',#10391,10.);
#4311=CIRCLE('',#10392,10.);
#4312=CIRCLE('',#10393,10.);
#4313=CIRCLE('',#10394,10.);
#4314=CIRCLE('',#10395,10.);
#4795=VERTEX_POINT('',#14754);
#4796=VERTEX_POINT('',#14756);
#4797=VERTEX_POINT('',#14758);
#4798=VERTEX_POINT('',#14797);
#4799=VERTEX_POINT('',#14798);
#4800=VERTEX_POINT('',#14817);
#4801=VERTEX_POINT('',#14840);
#4802=VERTEX_POINT('',#14842);
#4803=VERTEX_POINT('',#14846);
#4804=VERTEX_POINT('',#14848);
#4805=VERTEX_POINT('',#14852);
#4806=VERTEX_POINT('',#14853);
#4807=VERTEX_POINT('',#14855);
#4808=VERTEX_POINT('',#14857);
#4809=VERTEX_POINT('',#14859);
#4810=VERTEX_POINT('',#14861);
#4811=VERTEX_POINT('',#14864);
#4812=VERTEX_POINT('',#14867);
#4813=VERTEX_POINT('',#14869);
#4814=VERTEX_POINT('',#14871);
#5821=EDGE_CURVE('',#4795,#4795,#4303,.T.);
#5822=EDGE_CURVE('',#4795,#4796,#2566,.T.);
#5823=EDGE_CURVE('',#4796,#4797,#189,.T.);
#5824=EDGE_CURVE('',#4797,#4796,#190,.T.);
#5825=EDGE_CURVE('',#4798,#4799,#191,.T.);
#5826=EDGE_CURVE('',#4799,#4800,#2567,.T.);
#5827=EDGE_CURVE('',#4800,#4800,#4304,.T.);
#5828=EDGE_CURVE('',#4799,#4798,#192,.T.);
#5829=EDGE_CURVE('',#4801,#4801,#4305,.T.);
#5830=EDGE_CURVE('',#4801,#4802,#2568,.T.);
#5831=EDGE_CURVE('',#4802,#4802,#4306,.T.);
#5832=EDGE_CURVE('',#4803,#4803,#4307,.T.);
#5833=EDGE_CURVE('',#4803,#4804,#2569,.T.);
#5834=EDGE_CURVE('',#4804,#4804,#4308,.T.);
#5835=EDGE_CURVE('',#4805,#4806,#4309,.T.);
#5836=EDGE_CURVE('',#4807,#4805,#2570,.T.);
#5837=EDGE_CURVE('',#4807,#4808,#4310,.T.);
#5838=EDGE_CURVE('',#4809,#4808,#2571,.T.);
#5839=EDGE_CURVE('',#4810,#4809,#4311,.T.);
#5840=EDGE_CURVE('',#4810,#4799,#2572,.T.);
#5841=EDGE_CURVE('',#4798,#4811,#2573,.T.);
#5842=EDGE_CURVE('',#4811,#4811,#4312,.T.);
#5843=EDGE_CURVE('',#4812,#4810,#4313,.T.);
#5844=EDGE_CURVE('',#4813,#4812,#2574,.T.);
#5845=EDGE_CURVE('',#4813,#4814,#4314,.T.);
#5846=EDGE_CURVE('',#4806,#4814,#2575,.T.);
#5847=EDGE_CURVE('',#4805,#4806,#2576,.T.);
#5848=EDGE_CURVE('',#4812,#4809,#2577,.T.);
#5849=EDGE_CURVE('',#4814,#4807,#2578,.T.);
#5850=EDGE_CURVE('',#4808,#4813,#2579,.T.);
#7617=ORIENTED_EDGE('',*,*,#5821,.F.);
#7618=ORIENTED_EDGE('',*,*,#5822,.T.);
#7619=ORIENTED_EDGE('',*,*,#5823,.T.);
#7620=ORIENTED_EDGE('',*,*,#5824,.T.);
#7621=ORIENTED_EDGE('',*,*,#5822,.F.);
#7622=ORIENTED_EDGE('',*,*,#5825,.T.);
#7623=ORIENTED_EDGE('',*,*,#5826,.T.);
#7624=ORIENTED_EDGE('',*,*,#5827,.F.);
#7625=ORIENTED_EDGE('',*,*,#5826,.F.);
#7626=ORIENTED_EDGE('',*,*,#5828,.T.);
#7627=ORIENTED_EDGE('',*,*,#5829,.F.);
#7628=ORIENTED_EDGE('',*,*,#5830,.T.);
#7629=ORIENTED_EDGE('',*,*,#5831,.T.);
#7630=ORIENTED_EDGE('',*,*,#5830,.F.);
#7631=ORIENTED_EDGE('',*,*,#5832,.F.);
#7632=ORIENTED_EDGE('',*,*,#5833,.T.);
#7633=ORIENTED_EDGE('',*,*,#5834,.T.);
#7634=ORIENTED_EDGE('',*,*,#5833,.F.);
#7635=ORIENTED_EDGE('',*,*,#5835,.F.);
#7636=ORIENTED_EDGE('',*,*,#5836,.F.);
#7637=ORIENTED_EDGE('',*,*,#5837,.T.);
#7638=ORIENTED_EDGE('',*,*,#5838,.F.);
#7639=ORIENTED_EDGE('',*,*,#5839,.F.);
#7640=ORIENTED_EDGE('',*,*,#5840,.T.);
#7641=ORIENTED_EDGE('',*,*,#5825,.F.);
#7642=ORIENTED_EDGE('',*,*,#5841,.T.);
#7643=ORIENTED_EDGE('',*,*,#5842,.T.);
#7644=ORIENTED_EDGE('',*,*,#5841,.F.);
#7645=ORIENTED_EDGE('',*,*,#5828,.F.);
#7646=ORIENTED_EDGE('',*,*,#5840,.F.);
#7647=ORIENTED_EDGE('',*,*,#5843,.F.);
#7648=ORIENTED_EDGE('',*,*,#5844,.F.);
#7649=ORIENTED_EDGE('',*,*,#5845,.T.);
#7650=ORIENTED_EDGE('',*,*,#5846,.F.);
#7651=ORIENTED_EDGE('',*,*,#5824,.F.);
#7652=ORIENTED_EDGE('',*,*,#5823,.F.);
#7653=ORIENTED_EDGE('',*,*,#5847,.F.);
#7654=ORIENTED_EDGE('',*,*,#5835,.T.);
#7655=ORIENTED_EDGE('',*,*,#5848,.F.);
#7656=ORIENTED_EDGE('',*,*,#5843,.T.);
#7657=ORIENTED_EDGE('',*,*,#5839,.T.);
#7658=ORIENTED_EDGE('',*,*,#5842,.F.);
#7659=ORIENTED_EDGE('',*,*,#5832,.T.);
#7660=ORIENTED_EDGE('',*,*,#5834,.F.);
#7661=ORIENTED_EDGE('',*,*,#5829,.T.);
#7662=ORIENTED_EDGE('',*,*,#5831,.F.);
#7663=ORIENTED_EDGE('',*,*,#5836,.T.);
#7664=ORIENTED_EDGE('',*,*,#5847,.T.);
#7665=ORIENTED_EDGE('',*,*,#5846,.T.);
#7666=ORIENTED_EDGE('',*,*,#5849,.T.);
#7667=ORIENTED_EDGE('',*,*,#5821,.T.);
#7668=ORIENTED_EDGE('',*,*,#5844,.T.);
#7669=ORIENTED_EDGE('',*,*,#5848,.T.);
#7670=ORIENTED_EDGE('',*,*,#5838,.T.);
#7671=ORIENTED_EDGE('',*,*,#5850,.T.);
#7672=ORIENTED_EDGE('',*,*,#5827,.T.);
#7673=ORIENTED_EDGE('',*,*,#5850,.F.);
#7674=ORIENTED_EDGE('',*,*,#5837,.F.);
#7675=ORIENTED_EDGE('',*,*,#5849,.F.);
#7676=ORIENTED_EDGE('',*,*,#5845,.F.);
#9203=CYLINDRICAL_SURFACE('',#10379,2.2);
#9204=CYLINDRICAL_SURFACE('',#10381,2.2);
#9205=CYLINDRICAL_SURFACE('',#10383,6.);
#9206=CYLINDRICAL_SURFACE('',#10386,8.75);
#9207=CYLINDRICAL_SURFACE('',#10389,10.);
#9448=ADVANCED_FACE('',(#1123),#9203,.F.);
#9449=ADVANCED_FACE('',(#1124),#9204,.F.);
#9450=ADVANCED_FACE('',(#1125),#9205,.T.);
#9451=ADVANCED_FACE('',(#1126),#9206,.T.);
#9452=ADVANCED_FACE('',(#1127,#350),#9207,.T.);
#9453=ADVANCED_FACE('',(#1128),#607,.F.);
#9454=ADVANCED_FACE('',(#1129),#608,.F.);
#9455=ADVANCED_FACE('',(#1130,#351),#609,.F.);
#9456=ADVANCED_FACE('',(#1131,#352),#610,.F.);
#9457=ADVANCED_FACE('',(#1132),#611,.F.);
#9458=ADVANCED_FACE('',(#1133,#353),#612,.T.);
#9459=ADVANCED_FACE('',(#1134,#354),#613,.T.);
#9460=ADVANCED_FACE('',(#1135),#614,.F.);
#9796=CLOSED_SHELL('',(#9448,#9449,#9450,#9451,#9452,#9453,#9454,#9455,
#9456,#9457,#9458,#9459,#9460));
#10378=AXIS2_PLACEMENT_3D('',#14752,#11962,#11963);
#10379=AXIS2_PLACEMENT_3D('',#14753,#11964,#11965);
#10380=AXIS2_PLACEMENT_3D('',#14755,#11966,#11967);
#10381=AXIS2_PLACEMENT_3D('',#14796,#11969,#11970);
#10382=AXIS2_PLACEMENT_3D('',#14819,#11972,#11973);
#10383=AXIS2_PLACEMENT_3D('',#14839,#11974,#11975);
#10384=AXIS2_PLACEMENT_3D('',#14841,#11976,#11977);
#10385=AXIS2_PLACEMENT_3D('',#14844,#11979,#11980);
#10386=AXIS2_PLACEMENT_3D('',#14845,#11981,#11982);
#10387=AXIS2_PLACEMENT_3D('',#14847,#11983,#11984);
#10388=AXIS2_PLACEMENT_3D('',#14850,#11986,#11987);
#10389=AXIS2_PLACEMENT_3D('',#14851,#11988,#11989);
#10390=AXIS2_PLACEMENT_3D('',#14854,#11990,#11991);
#10391=AXIS2_PLACEMENT_3D('',#14858,#11993,#11994);
#10392=AXIS2_PLACEMENT_3D('',#14862,#11996,#11997);
#10393=AXIS2_PLACEMENT_3D('',#14866,#12000,#12001);
#10394=AXIS2_PLACEMENT_3D('',#14868,#12002,#12003);
#10395=AXIS2_PLACEMENT_3D('',#14872,#12005,#12006);
#10396=AXIS2_PLACEMENT_3D('',#14874,#12008,#12009);
#10397=AXIS2_PLACEMENT_3D('',#14876,#12011,#12012);
#10398=AXIS2_PLACEMENT_3D('',#14878,#12014,#12015);
#10399=AXIS2_PLACEMENT_3D('',#14879,#12016,#12017);
#10400=AXIS2_PLACEMENT_3D('',#14880,#12018,#12019);
#10401=AXIS2_PLACEMENT_3D('',#14881,#12020,#12021);
#10402=AXIS2_PLACEMENT_3D('',#14883,#12023,#12024);
#10403=AXIS2_PLACEMENT_3D('',#14885,#12026,#12027);
#11962=DIRECTION('axis',(0.,0.,1.));
#11963=DIRECTION('refdir',(1.,0.,0.));
#11964=DIRECTION('center_axis',(-1.,0.,0.));
#11965=DIRECTION('ref_axis',(0.,0.,1.));
#11966=DIRECTION('center_axis',(-1.,0.,0.));
#11967=DIRECTION('ref_axis',(0.,0.,-1.));
#11968=DIRECTION('',(-1.,0.,0.));
#11969=DIRECTION('center_axis',(-1.,0.,0.));
#11970=DIRECTION('ref_axis',(0.,0.,1.));
#11971=DIRECTION('',(-1.,0.,0.));
#11972=DIRECTION('center_axis',(1.,0.,0.));
#11973=DIRECTION('ref_axis',(0.,0.,1.));
#11974=DIRECTION('center_axis',(0.,0.,-1.));
#11975=DIRECTION('ref_axis',(-1.,0.,0.));
#11976=DIRECTION('center_axis',(0.,0.,-1.));
#11977=DIRECTION('ref_axis',(-1.,0.,0.));
#11978=DIRECTION('',(0.,0.,1.));
#11979=DIRECTION('center_axis',(0.,0.,-1.));
#11980=DIRECTION('ref_axis',(-1.,0.,0.));
#11981=DIRECTION('center_axis',(0.,0.,-1.));
#11982=DIRECTION('ref_axis',(-1.,0.,0.));
#11983=DIRECTION('center_axis',(0.,0.,-1.));
#11984=DIRECTION('ref_axis',(-1.,0.,0.));
#11985=DIRECTION('',(0.,0.,1.));
#11986=DIRECTION('center_axis',(0.,0.,-1.));
#11987=DIRECTION('ref_axis',(-1.,0.,0.));
#11988=DIRECTION('center_axis',(0.,0.,-1.));
#11989=DIRECTION('ref_axis',(-1.,0.,0.));
#11990=DIRECTION('center_axis',(0.,0.,-1.));
#11991=DIRECTION('ref_axis',(-1.,0.,0.));
#11992=DIRECTION('',(0.,0.,-1.));
#11993=DIRECTION('center_axis',(0.,0.,1.));
#11994=DIRECTION('ref_axis',(1.,0.,0.));
#11995=DIRECTION('',(0.,0.,1.));
#11996=DIRECTION('center_axis',(0.,0.,-1.));
#11997=DIRECTION('ref_axis',(-1.,0.,0.));
#11998=DIRECTION('',(0.,0.,1.));
#11999=DIRECTION('',(0.,0.,1.));
#12000=DIRECTION('center_axis',(0.,0.,-1.));
#12001=DIRECTION('ref_axis',(-1.,0.,0.));
#12002=DIRECTION('center_axis',(0.,0.,-1.));
#12003=DIRECTION('ref_axis',(-1.,0.,0.));
#12004=DIRECTION('',(0.,0.,-1.));
#12005=DIRECTION('center_axis',(0.,0.,1.));
#12006=DIRECTION('ref_axis',(1.,0.,0.));
#12007=DIRECTION('',(0.,0.,1.));
#12008=DIRECTION('center_axis',(0.,0.,1.));
#12009=DIRECTION('ref_axis',(1.,0.,0.));
#12010=DIRECTION('',(0.,1.,0.));
#12011=DIRECTION('center_axis',(0.,0.,1.));
#12012=DIRECTION('ref_axis',(1.,0.,0.));
#12013=DIRECTION('',(0.,-1.,0.));
#12014=DIRECTION('center_axis',(0.,0.,-1.));
#12015=DIRECTION('ref_axis',(-1.,0.,0.));
#12016=DIRECTION('center_axis',(0.,0.,-1.));
#12017=DIRECTION('ref_axis',(-1.,0.,0.));
#12018=DIRECTION('center_axis',(0.,0.,-1.));
#12019=DIRECTION('ref_axis',(-1.,0.,0.));
#12020=DIRECTION('center_axis',(1.,0.,0.));
#12021=DIRECTION('ref_axis',(0.,0.,-1.));
#12022=DIRECTION('',(0.,-1.,0.));
#12023=DIRECTION('center_axis',(-1.,0.,0.));
#12024=DIRECTION('ref_axis',(0.,0.,1.));
#12025=DIRECTION('',(0.,1.,0.));
#12026=DIRECTION('center_axis',(0.,0.,1.));
#12027=DIRECTION('ref_axis',(1.,0.,0.));
#14752=CARTESIAN_POINT('',(0.,0.,0.));
#14753=CARTESIAN_POINT('Origin',(12.,0.,11.));
#14754=CARTESIAN_POINT('',(-3.2,-2.69422295812418E-16,8.8));
#14755=CARTESIAN_POINT('Origin',(-3.2,0.,11.));
#14756=CARTESIAN_POINT('',(-10.,-2.69422295812418E-16,8.8));
#14757=CARTESIAN_POINT('',(12.,-2.69422295812418E-16,8.8));
#14758=CARTESIAN_POINT('',(-10.,4.3528800643699E-16,13.2));
#14759=CARTESIAN_POINT('Ctrl Pts',(-10.,-2.77555756156289E-16,8.8));
#14760=CARTESIAN_POINT('Ctrl Pts',(-10.,-0.277203807947464,8.8));
#14761=CARTESIAN_POINT('Ctrl Pts',(-9.98731242652721,-0.572272533644394,
8.85558441201917));
#14762=CARTESIAN_POINT('Ctrl Pts',(-9.94146891308711,-1.1140472218706,9.08038732993933));
#14763=CARTESIAN_POINT('Ctrl Pts',(-9.90893754512743,-1.36082632626377,
9.24955648904296));
#14764=CARTESIAN_POINT('Ctrl Pts',(-9.84757782914463,-1.75045962433893,
9.63918978711812));
#14765=CARTESIAN_POINT('Ctrl Pts',(-9.81469565126959,-1.91961618195498,
9.88596209803831));
#14766=CARTESIAN_POINT('Ctrl Pts',(-9.76804398559235,-2.14440993937815,
10.4277129969916));
#14767=CARTESIAN_POINT('Ctrl Pts',(-9.75499871860576,-2.2,10.7227732634396));
#14768=CARTESIAN_POINT('Ctrl Pts',(-9.75499871860576,-2.2,11.2772267365604));
#14769=CARTESIAN_POINT('Ctrl Pts',(-9.76804398559235,-2.14440993937815,
11.5722870030084));
#14770=CARTESIAN_POINT('Ctrl Pts',(-9.81469565126959,-1.91961618195498,
12.1140379019617));
#14771=CARTESIAN_POINT('Ctrl Pts',(-9.84757782914463,-1.75045962433893,
12.3608102128819));
#14772=CARTESIAN_POINT('Ctrl Pts',(-9.90893754512743,-1.36082632626377,
12.750443510957));
#14773=CARTESIAN_POINT('Ctrl Pts',(-9.94146891308711,-1.1140472218706,12.9196126700607));
#14774=CARTESIAN_POINT('Ctrl Pts',(-9.98731242652721,-0.572272533644395,
13.1444155879808));
#14775=CARTESIAN_POINT('Ctrl Pts',(-10.,-0.277203807947464,13.2));
#14776=CARTESIAN_POINT('Ctrl Pts',(-10.,-2.08166817117217E-16,13.2));
#14777=CARTESIAN_POINT('Ctrl Pts',(-10.,-2.08166817117217E-16,13.2));
#14778=CARTESIAN_POINT('Ctrl Pts',(-10.,0.277203807947464,13.2));
#14779=CARTESIAN_POINT('Ctrl Pts',(-9.98731242652721,0.572272533644394,
13.1444155879808));
#14780=CARTESIAN_POINT('Ctrl Pts',(-9.94146891308711,1.1140472218706,12.9196126700607));
#14781=CARTESIAN_POINT('Ctrl Pts',(-9.90893754512743,1.36082632626377,12.750443510957));
#14782=CARTESIAN_POINT('Ctrl Pts',(-9.84757782914463,1.75045962433893,12.3608102128819));
#14783=CARTESIAN_POINT('Ctrl Pts',(-9.81469565126959,1.91961618195498,12.1140379019617));
#14784=CARTESIAN_POINT('Ctrl Pts',(-9.76804398559235,2.14440993937815,11.5722870030084));
#14785=CARTESIAN_POINT('Ctrl Pts',(-9.75499871860576,2.2,11.2772267365604));
#14786=CARTESIAN_POINT('Ctrl Pts',(-9.75499871860576,2.2,11.));
#14787=CARTESIAN_POINT('Ctrl Pts',(-9.75499871860576,2.2,10.7227732634396));
#14788=CARTESIAN_POINT('Ctrl Pts',(-9.76804398559235,2.14440993937815,10.4277129969916));
#14789=CARTESIAN_POINT('Ctrl Pts',(-9.81469565126959,1.91961618195498,9.88596209803831));
#14790=CARTESIAN_POINT('Ctrl Pts',(-9.84757782914463,1.75045962433893,9.63918978711812));
#14791=CARTESIAN_POINT('Ctrl Pts',(-9.90893754512743,1.36082632626377,9.24955648904296));
#14792=CARTESIAN_POINT('Ctrl Pts',(-9.94146891308711,1.1140472218706,9.08038732993933));
#14793=CARTESIAN_POINT('Ctrl Pts',(-9.98731242652721,0.572272533644394,
8.85558441201917));
#14794=CARTESIAN_POINT('Ctrl Pts',(-10.,0.277203807947463,8.8));
#14795=CARTESIAN_POINT('Ctrl Pts',(-10.,-4.16333634234434E-16,8.8));
#14796=CARTESIAN_POINT('Origin',(12.,0.,11.));
#14797=CARTESIAN_POINT('',(10.,-4.3528800643699E-16,13.2));
#14798=CARTESIAN_POINT('',(10.,-2.69422295812418E-16,8.8));
#14799=CARTESIAN_POINT('Ctrl Pts',(10.,-5.55111512312578E-16,13.2));
#14800=CARTESIAN_POINT('Ctrl Pts',(10.,-0.277203807947464,13.2));
#14801=CARTESIAN_POINT('Ctrl Pts',(9.98731242652721,-0.572272533644394,
13.1444155879808));
#14802=CARTESIAN_POINT('Ctrl Pts',(9.94146891308711,-1.1140472218706,12.9196126700607));
#14803=CARTESIAN_POINT('Ctrl Pts',(9.90893754512743,-1.36082632626377,12.750443510957));
#14804=CARTESIAN_POINT('Ctrl Pts',(9.84757782914463,-1.75045962433893,12.3608102128819));
#14805=CARTESIAN_POINT('Ctrl Pts',(9.81469565126959,-1.91961618195498,12.1140379019617));
#14806=CARTESIAN_POINT('Ctrl Pts',(9.76804398559235,-2.14440993937815,11.5722870030084));
#14807=CARTESIAN_POINT('Ctrl Pts',(9.75499871860576,-2.2,11.2772267365605));
#14808=CARTESIAN_POINT('Ctrl Pts',(9.75499871860576,-2.2,10.7227732634396));
#14809=CARTESIAN_POINT('Ctrl Pts',(9.76804398559235,-2.14440993937815,10.4277129969916));
#14810=CARTESIAN_POINT('Ctrl Pts',(9.81469565126959,-1.91961618195498,9.88596209803831));
#14811=CARTESIAN_POINT('Ctrl Pts',(9.84757782914463,-1.75045962433893,9.63918978711812));
#14812=CARTESIAN_POINT('Ctrl Pts',(9.90893754512743,-1.36082632626377,9.24955648904296));
#14813=CARTESIAN_POINT('Ctrl Pts',(9.94146891308711,-1.1140472218706,9.08038732993933));
#14814=CARTESIAN_POINT('Ctrl Pts',(9.98731242652721,-0.572272533644394,
8.85558441201917));
#14815=CARTESIAN_POINT('Ctrl Pts',(10.,-0.277203807947463,8.8));
#14816=CARTESIAN_POINT('Ctrl Pts',(10.,4.16333634234434E-16,8.8));
#14817=CARTESIAN_POINT('',(3.2,-2.69422295812418E-16,8.8));
#14818=CARTESIAN_POINT('',(12.,-2.69422295812418E-16,8.8));
#14819=CARTESIAN_POINT('Origin',(3.2,0.,11.));
#14820=CARTESIAN_POINT('Ctrl Pts',(10.,1.38777878078145E-16,8.8));
#14821=CARTESIAN_POINT('Ctrl Pts',(10.,0.277203807947464,8.8));
#14822=CARTESIAN_POINT('Ctrl Pts',(9.98731242652721,0.572272533644394,8.85558441201917));
#14823=CARTESIAN_POINT('Ctrl Pts',(9.94146891308711,1.1140472218706,9.08038732993933));
#14824=CARTESIAN_POINT('Ctrl Pts',(9.90893754512743,1.36082632626377,9.24955648904296));
#14825=CARTESIAN_POINT('Ctrl Pts',(9.84757782914463,1.75045962433893,9.63918978711812));
#14826=CARTESIAN_POINT('Ctrl Pts',(9.81469565126959,1.91961618195498,9.88596209803831));
#14827=CARTESIAN_POINT('Ctrl Pts',(9.76804398559235,2.14440993937815,10.4277129969916));
#14828=CARTESIAN_POINT('Ctrl Pts',(9.75499871860576,2.2,10.7227732634396));
#14829=CARTESIAN_POINT('Ctrl Pts',(9.75499871860576,2.2,11.));
#14830=CARTESIAN_POINT('Ctrl Pts',(9.75499871860576,2.2,11.2772267365604));
#14831=CARTESIAN_POINT('Ctrl Pts',(9.76804398559235,2.14440993937815,11.5722870030084));
#14832=CARTESIAN_POINT('Ctrl Pts',(9.81469565126959,1.91961618195498,12.1140379019617));
#14833=CARTESIAN_POINT('Ctrl Pts',(9.84757782914463,1.75045962433893,12.3608102128819));
#14834=CARTESIAN_POINT('Ctrl Pts',(9.90893754512743,1.36082632626377,12.750443510957));
#14835=CARTESIAN_POINT('Ctrl Pts',(9.94146891308711,1.1140472218706,12.9196126700607));
#14836=CARTESIAN_POINT('Ctrl Pts',(9.98731242652721,0.572272533644393,13.1444155879808));
#14837=CARTESIAN_POINT('Ctrl Pts',(10.,0.277203807947463,13.2));
#14838=CARTESIAN_POINT('Ctrl Pts',(10.,-6.24500451351651E-16,13.2));
#14839=CARTESIAN_POINT('Origin',(0.,0.,-5.));
#14840=CARTESIAN_POINT('',(6.,-7.34788079488412E-16,172.));
#14841=CARTESIAN_POINT('Origin',(0.,0.,172.));
#14842=CARTESIAN_POINT('',(6.,-7.34788079488412E-16,190.));
#14843=CARTESIAN_POINT('',(6.,-7.34788079488412E-16,-5.));
#14844=CARTESIAN_POINT('Origin',(0.,0.,190.));
#14845=CARTESIAN_POINT('Origin',(0.,0.,-5.));
#14846=CARTESIAN_POINT('',(8.75,-1.07156594925393E-15,23.));
#14847=CARTESIAN_POINT('Origin',(0.,0.,23.));
#14848=CARTESIAN_POINT('',(8.75,-1.07156594925393E-15,172.));
#14849=CARTESIAN_POINT('',(8.75,-1.07156594925393E-15,-5.));
#14850=CARTESIAN_POINT('Origin',(0.,0.,172.));
#14851=CARTESIAN_POINT('Origin',(0.,0.,-5.));
#14852=CARTESIAN_POINT('',(-3.2,-9.47417542586161,0.));
#14853=CARTESIAN_POINT('',(-3.2,9.47417542586161,0.));
#14854=CARTESIAN_POINT('Origin',(0.,0.,0.));
#14855=CARTESIAN_POINT('',(-3.2,-9.47417542586161,20.));
#14856=CARTESIAN_POINT('',(-3.2,-9.47417542586161,-5.));
#14857=CARTESIAN_POINT('',(3.2,-9.47417542586161,20.));
#14858=CARTESIAN_POINT('Origin',(0.,0.,20.));
#14859=CARTESIAN_POINT('',(3.2,-9.47417542586161,0.));
#14860=CARTESIAN_POINT('',(3.2,-9.47417542586161,-5.));
#14861=CARTESIAN_POINT('',(10.,-1.22464679914735E-15,0.));
#14862=CARTESIAN_POINT('Origin',(0.,0.,0.));
#14863=CARTESIAN_POINT('',(10.,-1.22464679914735E-15,-5.));
#14864=CARTESIAN_POINT('',(10.,-1.22464679914735E-15,23.));
#14865=CARTESIAN_POINT('',(10.,-1.22464679914735E-15,-5.));
#14866=CARTESIAN_POINT('Origin',(0.,0.,23.));
#14867=CARTESIAN_POINT('',(3.2,9.47417542586161,0.));
#14868=CARTESIAN_POINT('Origin',(0.,0.,0.));
#14869=CARTESIAN_POINT('',(3.2,9.47417542586161,20.));
#14870=CARTESIAN_POINT('',(3.2,9.47417542586161,-5.));
#14871=CARTESIAN_POINT('',(-3.2,9.47417542586161,20.));
#14872=CARTESIAN_POINT('Origin',(0.,0.,20.));
#14873=CARTESIAN_POINT('',(-3.2,9.47417542586161,-5.));
#14874=CARTESIAN_POINT('Origin',(0.,0.,0.));
#14875=CARTESIAN_POINT('',(-3.2,0.,0.));
#14876=CARTESIAN_POINT('Origin',(0.,0.,0.));
#14877=CARTESIAN_POINT('',(3.2,0.,0.));
#14878=CARTESIAN_POINT('Origin',(10.,0.,23.));
#14879=CARTESIAN_POINT('Origin',(8.75,0.,172.));
#14880=CARTESIAN_POINT('Origin',(6.,0.,190.));
#14881=CARTESIAN_POINT('Origin',(-3.2,11.,20.));
#14882=CARTESIAN_POINT('',(-3.2,11.,20.));
#14883=CARTESIAN_POINT('Origin',(3.2,-11.,20.));
#14884=CARTESIAN_POINT('',(3.2,-11.,20.));
#14885=CARTESIAN_POINT('Origin',(0.,0.,20.));
#16557=UNCERTAINTY_MEASURE_WITH_UNIT(LENGTH_MEASURE(0.01),#16599,
'DISTANCE_ACCURACY_VALUE',
'Maximum model space distance between geometric entities at asserted c
onnectivities');
#16572=UNCERTAINTY_MEASURE_WITH_UNIT(LENGTH_MEASURE(0.01),#16599,
'DISTANCE_ACCURACY_VALUE',
'Maximum model space distance between geometric entities at asserted c
onnectivities');
#16583=(
GEOMETRIC_REPRESENTATION_CONTEXT(3)
GLOBAL_UNCERTAINTY_ASSIGNED_CONTEXT((#16557))
GLOBAL_UNIT_ASSIGNED_CONTEXT((#16599,#16601,#16602))
REPRESENTATION_CONTEXT('','3D')
);
#16598=(
GEOMETRIC_REPRESENTATION_CONTEXT(3)
GLOBAL_UNCERTAINTY_ASSIGNED_CONTEXT((#16572))
GLOBAL_UNIT_ASSIGNED_CONTEXT((#16599,#16601,#16602))
REPRESENTATION_CONTEXT('','3D')
);
#16599=(
LENGTH_UNIT()
NAMED_UNIT(*)
SI_UNIT(.MILLI.,.METRE.)
);
#16601=(
NAMED_UNIT(*)
PLANE_ANGLE_UNIT()
SI_UNIT($,.RADIAN.)
);
#16602=(
NAMED_UNIT(*)
SI_UNIT($,.STERADIAN.)
SOLID_ANGLE_UNIT()
);
#16613=SHAPE_DEFINITION_REPRESENTATION(#16638,#16707);
#16638=PRODUCT_DEFINITION_SHAPE('',$,#16733);
#16707=SHAPE_REPRESENTATION('',(#10378),#16583);
#16722=PRODUCT_DEFINITION_CONTEXT('part definition',#16799,'design');
#16733=PRODUCT_DEFINITION('P12_Jaw_Clamping_Screw',
'P12_Jaw_Clamping_Screw',#16758,#16722);
#16758=PRODUCT_DEFINITION_FORMATION('',$,#16811);
#16799=APPLICATION_CONTEXT(
'Core Data for Automotive Mechanical Design Process');
#16800=PRODUCT_CONTEXT('part definition',#16799,'mechanical');
#16811=PRODUCT('P12_Jaw_Clamping_Screw','P12_Jaw_Clamping_Screw',$,(#16800));
#16833=PRESENTATION_STYLE_ASSIGNMENT((#16842));
#16842=SURFACE_STYLE_USAGE(.BOTH.,#16851);
#16851=SURFACE_SIDE_STYLE('',(#16860));
#16860=SURFACE_STYLE_FILL_AREA(#16869);
#16869=FILL_AREA_STYLE('Blue',(#16878));
#16878=FILL_AREA_STYLE_COLOUR('Blue',#16887);
#16887=COLOUR_RGB('Blue',0.,0.4,0.8);
ENDSEC;
END-ISO-10303-21;
